ISO-10303-21;
HEADER;
/* Generated by software containing ST-Developer
 * from STEP Tools, Inc. (www.steptools.com) 
 */

FILE_DESCRIPTION(
/* description */ ('Indexing fixture plate with plunger'),
/* implementation_level */ '2;1');

FILE_NAME(
/* name */ 'M6x18 mounting screw.step',
/* time_stamp */ '2026-10-28T03:23:41-07:00',
/* author */ (''),
/* organization */ (''),
/* preprocessor_version */ 'ST-DEVELOPER v20.2',
/* originating_system */ 'Autodesk Translation Framework v15.17.0.0',
/* authorisation */ '');

FILE_SCHEMA (('AUTOMOTIVE_DESIGN { 1 0 10303 214 3 1 1 }'));
ENDSEC;

DATA;
#10=MECHANICAL_DESIGN_GEOMETRIC_PRESENTATION_REPRESENTATION('',(#329),#10020);
#215=CONICAL_SURFACE('',#5073,0.475,0.785398163397449);
#216=CONICAL_SURFACE('',#5077,0.485,0.785398163397448);
#217=CONICAL_SURFACE('',#5081,0.31,0.463647609000806);
#229=ORIENTED_CLOSED_SHELL('',*,#4583,.F.);
#231=BREP_WITH_VOIDS('Body1',#4584,(#229));
#275=SHAPE_REPRESENTATION_RELATIONSHIP('SRR','None',#10149,#302);
#302=ADVANCED_BREP_SHAPE_REPRESENTATION('',(#231),#10002);
#329=STYLED_ITEM('',(#10375),#231);
#430=FACE_BOUND('',#1083,.T.);
#572=PLANE('',#5061);
#573=PLANE('',#5062);
#574=PLANE('',#5063);
#575=PLANE('',#5064);
#576=PLANE('',#5065);
#577=PLANE('',#5066);
#578=PLANE('',#5067);
#579=PLANE('',#5068);
#580=PLANE('',#5069);
#581=PLANE('',#5071);
#582=PLANE('',#5079);
#740=FACE_OUTER_BOUND('',#1069,.T.);
#741=FACE_OUTER_BOUND('',#1070,.T.);
#742=FACE_OUTER_BOUND('',#1071,.T.);
#743=FACE_OUTER_BOUND('',#1072,.T.);
#744=FACE_OUTER_BOUND('',#1073,.T.);
#745=FACE_OUTER_BOUND('',#1074,.T.);
#746=FACE_OUTER_BOUND('',#1075,.T.);
#747=FACE_OUTER_BOUND('',#1076,.T.);
#748=FACE_OUTER_BOUND('',#1077,.T.);
#749=FACE_OUTER_BOUND('',#1078,.T.);
#750=FACE_OUTER_BOUND('',#1079,.T.);
#751=FACE_OUTER_BOUND('',#1080,.T.);
#752=FACE_OUTER_BOUND('',#1081,.T.);
#753=FACE_OUTER_BOUND('',#1082,.T.);
#754=FACE_OUTER_BOUND('',#1084,.T.);
#755=FACE_OUTER_BOUND('',#1085,.T.);
#1069=EDGE_LOOP('',(#3311,#3312,#3313,#3314));
#1070=EDGE_LOOP('',(#3315,#3316,#3317,#3318));
#1071=EDGE_LOOP('',(#3319,#3320,#3321,#3322));
#1072=EDGE_LOOP('',(#3323,#3324,#3325,#3326));
#1073=EDGE_LOOP('',(#3327,#3328,#3329,#3330));
#1074=EDGE_LOOP('',(#3331,#3332,#3333,#3334));
#1075=EDGE_LOOP('',(#3335,#3336,#3337,#3338,#3339,#3340));
#1076=EDGE_LOOP('',(#3341,#3342,#3343,#3344,#3345,#3346));
#1077=EDGE_LOOP('',(#3347));
#1078=EDGE_LOOP('',(#3348));
#1079=EDGE_LOOP('',(#3349,#3350,#3351,#3352));
#1080=EDGE_LOOP('',(#3353,#3354,#3355,#3356));
#1081=EDGE_LOOP('',(#3357,#3358,#3359,#3360));
#1082=EDGE_LOOP('',(#3361));
#1083=EDGE_LOOP('',(#3362));
#1084=EDGE_LOOP('',(#3363,#3364,#3365,#3366));
#1085=EDGE_LOOP('',(#3367,#3368,#3369,#3370));
#1440=LINE('',#8535,#1660);
#1441=LINE('',#8537,#1661);
#1442=LINE('',#8539,#1662);
#1443=LINE('',#8540,#1663);
#1444=LINE('',#8543,#1664);
#1445=LINE('',#8545,#1665);
#1446=LINE('',#8546,#1666);
#1447=LINE('',#8549,#1667);
#1448=LINE('',#8551,#1668);
#1449=LINE('',#8552,#1669);
#1450=LINE('',#8555,#1670);
#1451=LINE('',#8557,#1671);
#1452=LINE('',#8558,#1672);
#1453=LINE('',#8561,#1673);
#1454=LINE('',#8563,#1674);
#1455=LINE('',#8564,#1675);
#1456=LINE('',#8566,#1676);
#1457=LINE('',#8567,#1677);
#1458=LINE('',#8579,#1678);
#1459=LINE('',#8583,#1679);
#1460=LINE('',#8587,#1680);
#1461=LINE('',#8594,#1681);
#1462=LINE('',#8596,#1682);
#1660=VECTOR('',#5931,1.);
#1661=VECTOR('',#5932,1.);
#1662=VECTOR('',#5933,1.);
#1663=VECTOR('',#5934,1.);
#1664=VECTOR('',#5937,1.);
#1665=VECTOR('',#5938,1.);
#1666=VECTOR('',#5939,1.);
#1667=VECTOR('',#5942,1.);
#1668=VECTOR('',#5943,1.);
#1669=VECTOR('',#5944,1.);
#1670=VECTOR('',#5947,1.);
#1671=VECTOR('',#5948,1.);
#1672=VECTOR('',#5949,1.);
#1673=VECTOR('',#5952,1.);
#1674=VECTOR('',#5953,1.);
#1675=VECTOR('',#5954,1.);
#1676=VECTOR('',#5957,1.);
#1677=VECTOR('',#5958,1.);
#1678=VECTOR('',#5975,0.475);
#1679=VECTOR('',#5980,0.5);
#1680=VECTOR('',#5985,0.485);
#1681=VECTOR('',#5994,0.31);
#1682=VECTOR('',#5997,0.3);
#1902=CIRCLE('',#5070,0.2942);
#1903=CIRCLE('',#5072,0.45);
#1904=CIRCLE('',#5074,0.5);
#1905=CIRCLE('',#5076,0.5);
#1906=CIRCLE('',#5078,0.47);
#1907=CIRCLE('',#5080,0.32);
#1908=CIRCLE('',#5082,0.2942);
#2218=VERTEX_POINT('',#8533);
#2219=VERTEX_POINT('',#8534);
#2220=VERTEX_POINT('',#8536);
#2221=VERTEX_POINT('',#8538);
#2222=VERTEX_POINT('',#8542);
#2223=VERTEX_POINT('',#8544);
#2224=VERTEX_POINT('',#8548);
#2225=VERTEX_POINT('',#8550);
#2226=VERTEX_POINT('',#8554);
#2227=VERTEX_POINT('',#8556);
#2228=VERTEX_POINT('',#8560);
#2229=VERTEX_POINT('',#8562);
#2230=VERTEX_POINT('',#8571);
#2231=VERTEX_POINT('',#8574);
#2232=VERTEX_POINT('',#8577);
#2233=VERTEX_POINT('',#8581);
#2234=VERTEX_POINT('',#8585);
#2235=VERTEX_POINT('',#8589);
#2236=VERTEX_POINT('',#8592);
#2635=EDGE_CURVE('',#2218,#2219,#1440,.T.);
#2636=EDGE_CURVE('',#2219,#2220,#1441,.T.);
#2637=EDGE_CURVE('',#2220,#2221,#1442,.T.);
#2638=EDGE_CURVE('',#2218,#2221,#1443,.T.);
#2639=EDGE_CURVE('',#2219,#2222,#1444,.T.);
#2640=EDGE_CURVE('',#2222,#2223,#1445,.T.);
#2641=EDGE_CURVE('',#2223,#2220,#1446,.T.);
#2642=EDGE_CURVE('',#2222,#2224,#1447,.T.);
#2643=EDGE_CURVE('',#2224,#2225,#1448,.T.);
#2644=EDGE_CURVE('',#2225,#2223,#1449,.T.);
#2645=EDGE_CURVE('',#2224,#2226,#1450,.T.);
#2646=EDGE_CURVE('',#2226,#2227,#1451,.T.);
#2647=EDGE_CURVE('',#2227,#2225,#1452,.T.);
#2648=EDGE_CURVE('',#2226,#2228,#1453,.T.);
#2649=EDGE_CURVE('',#2228,#2229,#1454,.T.);
#2650=EDGE_CURVE('',#2229,#2227,#1455,.T.);
#2651=EDGE_CURVE('',#2228,#2218,#1456,.T.);
#2652=EDGE_CURVE('',#2221,#2229,#1457,.T.);
#2653=EDGE_CURVE('',#2230,#2230,#1902,.T.);
#2654=EDGE_CURVE('',#2231,#2231,#1903,.T.);
#2655=EDGE_CURVE('',#2232,#2232,#1904,.T.);
#2656=EDGE_CURVE('',#2232,#2231,#1458,.T.);
#2657=EDGE_CURVE('',#2233,#2233,#1905,.T.);
#2658=EDGE_CURVE('',#2233,#2232,#1459,.T.);
#2659=EDGE_CURVE('',#2234,#2234,#1906,.T.);
#2660=EDGE_CURVE('',#2234,#2233,#1460,.T.);
#2661=EDGE_CURVE('',#2235,#2235,#1907,.T.);
#2662=EDGE_CURVE('',#2236,#2236,#1908,.F.);
#2663=EDGE_CURVE('',#2236,#2235,#1461,.T.);
#2664=EDGE_CURVE('',#2230,#2236,#1462,.T.);
#3311=ORIENTED_EDGE('',*,*,#2635,.T.);
#3312=ORIENTED_EDGE('',*,*,#2636,.T.);
#3313=ORIENTED_EDGE('',*,*,#2637,.T.);
#3314=ORIENTED_EDGE('',*,*,#2638,.F.);
#3315=ORIENTED_EDGE('',*,*,#2639,.T.);
#3316=ORIENTED_EDGE('',*,*,#2640,.T.);
#3317=ORIENTED_EDGE('',*,*,#2641,.T.);
#3318=ORIENTED_EDGE('',*,*,#2636,.F.);
#3319=ORIENTED_EDGE('',*,*,#2642,.T.);
#3320=ORIENTED_EDGE('',*,*,#2643,.T.);
#3321=ORIENTED_EDGE('',*,*,#2644,.T.);
#3322=ORIENTED_EDGE('',*,*,#2640,.F.);
#3323=ORIENTED_EDGE('',*,*,#2645,.T.);
#3324=ORIENTED_EDGE('',*,*,#2646,.T.);
#3325=ORIENTED_EDGE('',*,*,#2647,.T.);
#3326=ORIENTED_EDGE('',*,*,#2643,.F.);
#3327=ORIENTED_EDGE('',*,*,#2648,.T.);
#3328=ORIENTED_EDGE('',*,*,#2649,.T.);
#3329=ORIENTED_EDGE('',*,*,#2650,.T.);
#3330=ORIENTED_EDGE('',*,*,#2646,.F.);
#3331=ORIENTED_EDGE('',*,*,#2651,.T.);
#3332=ORIENTED_EDGE('',*,*,#2638,.T.);
#3333=ORIENTED_EDGE('',*,*,#2652,.T.);
#3334=ORIENTED_EDGE('',*,*,#2649,.F.);
#3335=ORIENTED_EDGE('',*,*,#2651,.F.);
#3336=ORIENTED_EDGE('',*,*,#2648,.F.);
#3337=ORIENTED_EDGE('',*,*,#2645,.F.);
#3338=ORIENTED_EDGE('',*,*,#2642,.F.);
#3339=ORIENTED_EDGE('',*,*,#2639,.F.);
#3340=ORIENTED_EDGE('',*,*,#2635,.F.);
#3341=ORIENTED_EDGE('',*,*,#2652,.F.);
#3342=ORIENTED_EDGE('',*,*,#2637,.F.);
#3343=ORIENTED_EDGE('',*,*,#2641,.F.);
#3344=ORIENTED_EDGE('',*,*,#2644,.F.);
#3345=ORIENTED_EDGE('',*,*,#2647,.F.);
#3346=ORIENTED_EDGE('',*,*,#2650,.F.);
#3347=ORIENTED_EDGE('',*,*,#2653,.F.);
#3348=ORIENTED_EDGE('',*,*,#2654,.F.);
#3349=ORIENTED_EDGE('',*,*,#2655,.F.);
#3350=ORIENTED_EDGE('',*,*,#2656,.T.);
#3351=ORIENTED_EDGE('',*,*,#2654,.T.);
#3352=ORIENTED_EDGE('',*,*,#2656,.F.);
#3353=ORIENTED_EDGE('',*,*,#2657,.F.);
#3354=ORIENTED_EDGE('',*,*,#2658,.T.);
#3355=ORIENTED_EDGE('',*,*,#2655,.T.);
#3356=ORIENTED_EDGE('',*,*,#2658,.F.);
#3357=ORIENTED_EDGE('',*,*,#2659,.F.);
#3358=ORIENTED_EDGE('',*,*,#2660,.T.);
#3359=ORIENTED_EDGE('',*,*,#2657,.T.);
#3360=ORIENTED_EDGE('',*,*,#2660,.F.);
#3361=ORIENTED_EDGE('',*,*,#2659,.T.);
#3362=ORIENTED_EDGE('',*,*,#2661,.F.);
#3363=ORIENTED_EDGE('',*,*,#2662,.F.);
#3364=ORIENTED_EDGE('',*,*,#2663,.T.);
#3365=ORIENTED_EDGE('',*,*,#2661,.T.);
#3366=ORIENTED_EDGE('',*,*,#2663,.F.);
#3367=ORIENTED_EDGE('',*,*,#2653,.T.);
#3368=ORIENTED_EDGE('',*,*,#2664,.T.);
#3369=ORIENTED_EDGE('',*,*,#2662,.T.);
#3370=ORIENTED_EDGE('',*,*,#2664,.F.);
#4201=CYLINDRICAL_SURFACE('',#5075,0.5);
#4202=CYLINDRICAL_SURFACE('',#5083,0.2942);
#4355=ADVANCED_FACE('',(#740),#572,.F.);
#4356=ADVANCED_FACE('',(#741),#573,.F.);
#4357=ADVANCED_FACE('',(#742),#574,.F.);
#4358=ADVANCED_FACE('',(#743),#575,.F.);
#4359=ADVANCED_FACE('',(#744),#576,.F.);
#4360=ADVANCED_FACE('',(#745),#577,.F.);
#4361=ADVANCED_FACE('',(#746),#578,.F.);
#4362=ADVANCED_FACE('',(#747),#579,.F.);
#4363=ADVANCED_FACE('',(#748),#580,.F.);
#4364=ADVANCED_FACE('',(#749),#581,.T.);
#4365=ADVANCED_FACE('',(#750),#215,.T.);
#4366=ADVANCED_FACE('',(#751),#4201,.T.);
#4367=ADVANCED_FACE('',(#752),#216,.T.);
#4368=ADVANCED_FACE('',(#753,#430),#582,.T.);
#4369=ADVANCED_FACE('',(#754),#217,.T.);
#4370=ADVANCED_FACE('',(#755),#4202,.T.);
#4583=CLOSED_SHELL('',(#4355,#4356,#4357,#4358,#4359,#4360,#4361,#4362));
#4584=CLOSED_SHELL('',(#4363,#4364,#4365,#4366,#4367,#4368,#4369,#4370));
#5060=AXIS2_PLACEMENT_3D('',#8531,#5927,#5928);
#5061=AXIS2_PLACEMENT_3D('',#8532,#5929,#5930);
#5062=AXIS2_PLACEMENT_3D('',#8541,#5935,#5936);
#5063=AXIS2_PLACEMENT_3D('',#8547,#5940,#5941);
#5064=AXIS2_PLACEMENT_3D('',#8553,#5945,#5946);
#5065=AXIS2_PLACEMENT_3D('',#8559,#5950,#5951);
#5066=AXIS2_PLACEMENT_3D('',#8565,#5955,#5956);
#5067=AXIS2_PLACEMENT_3D('',#8568,#5959,#5960);
#5068=AXIS2_PLACEMENT_3D('',#8569,#5961,#5962);
#5069=AXIS2_PLACEMENT_3D('',#8570,#5963,#5964);
#5070=AXIS2_PLACEMENT_3D('',#8572,#5965,#5966);
#5071=AXIS2_PLACEMENT_3D('',#8573,#5967,#5968);
#5072=AXIS2_PLACEMENT_3D('',#8575,#5969,#5970);
#5073=AXIS2_PLACEMENT_3D('',#8576,#5971,#5972);
#5074=AXIS2_PLACEMENT_3D('',#8578,#5973,#5974);
#5075=AXIS2_PLACEMENT_3D('',#8580,#5976,#5977);
#5076=AXIS2_PLACEMENT_3D('',#8582,#5978,#5979);
#5077=AXIS2_PLACEMENT_3D('',#8584,#5981,#5982);
#5078=AXIS2_PLACEMENT_3D('',#8586,#5983,#5984);
#5079=AXIS2_PLACEMENT_3D('',#8588,#5986,#5987);
#5080=AXIS2_PLACEMENT_3D('',#8590,#5988,#5989);
#5081=AXIS2_PLACEMENT_3D('',#8591,#5990,#5991);
#5082=AXIS2_PLACEMENT_3D('',#8593,#5992,#5993);
#5083=AXIS2_PLACEMENT_3D('',#8595,#5995,#5996);
#5927=DIRECTION('axis',(0.,0.,1.));
#5928=DIRECTION('refdir',(1.,0.,0.));
#5929=DIRECTION('center_axis',(0.866025403784439,0.,-0.5));
#5930=DIRECTION('ref_axis',(0.5,0.,0.866025403784439));
#5931=DIRECTION('',(-0.5,0.,-0.866025403784439));
#5932=DIRECTION('',(0.,-1.,0.));
#5933=DIRECTION('',(0.5,0.,0.866025403784439));
#5934=DIRECTION('',(0.,-1.,0.));
#5935=DIRECTION('center_axis',(1.92296268638356E-16,0.,-1.));
#5936=DIRECTION('ref_axis',(1.,0.,1.92296268638356E-16));
#5937=DIRECTION('',(-1.,0.,-1.92296268638356E-16));
#5938=DIRECTION('',(0.,-1.,0.));
#5939=DIRECTION('',(1.,0.,1.92296268638356E-16));
#5940=DIRECTION('center_axis',(-0.866025403784439,0.,-0.5));
#5941=DIRECTION('ref_axis',(0.5,0.,-0.866025403784439));
#5942=DIRECTION('',(-0.5,0.,0.866025403784438));
#5943=DIRECTION('',(0.,-1.,0.));
#5944=DIRECTION('',(0.5,0.,-0.866025403784438));
#5945=DIRECTION('center_axis',(-0.866025403784439,0.,0.5));
#5946=DIRECTION('ref_axis',(-0.5,0.,-0.866025403784439));
#5947=DIRECTION('',(0.5,0.,0.866025403784439));
#5948=DIRECTION('',(0.,-1.,0.));
#5949=DIRECTION('',(-0.5,0.,-0.866025403784439));
#5950=DIRECTION('center_axis',(-1.92296268638356E-16,0.,1.));
#5951=DIRECTION('ref_axis',(-1.,0.,-1.92296268638356E-16));
#5952=DIRECTION('',(1.,0.,1.92296268638356E-16));
#5953=DIRECTION('',(0.,-1.,0.));
#5954=DIRECTION('',(-1.,0.,-1.92296268638356E-16));
#5955=DIRECTION('center_axis',(0.866025403784439,0.,0.5));
#5956=DIRECTION('ref_axis',(-0.5,0.,0.866025403784439));
#5957=DIRECTION('',(0.5,0.,-0.866025403784439));
#5958=DIRECTION('',(-0.5,0.,0.866025403784439));
#5959=DIRECTION('center_axis',(0.,1.,0.));
#5960=DIRECTION('ref_axis',(1.,0.,0.));
#5961=DIRECTION('center_axis',(0.,-1.,0.));
#5962=DIRECTION('ref_axis',(0.,0.,-1.));
#5963=DIRECTION('center_axis',(0.,1.,0.));
#5964=DIRECTION('ref_axis',(1.,0.,0.));
#5965=DIRECTION('center_axis',(0.,1.,0.));
#5966=DIRECTION('ref_axis',(1.,0.,0.));
#5967=DIRECTION('center_axis',(0.,1.,0.));
#5968=DIRECTION('ref_axis',(0.,0.,1.));
#5969=DIRECTION('center_axis',(0.,-1.,0.));
#5970=DIRECTION('ref_axis',(1.,0.,0.));
#5971=DIRECTION('center_axis',(0.,-1.,0.));
#5972=DIRECTION('ref_axis',(1.,0.,0.));
#5973=DIRECTION('center_axis',(0.,-1.,0.));
#5974=DIRECTION('ref_axis',(1.,0.,0.));
#5975=DIRECTION('',(0.707106781186548,0.707106781186547,8.65956056235494E-17));
#5976=DIRECTION('center_axis',(0.,-1.,0.));
#5977=DIRECTION('ref_axis',(1.,0.,0.));
#5978=DIRECTION('center_axis',(0.,-1.,0.));
#5979=DIRECTION('ref_axis',(1.,0.,0.));
#5980=DIRECTION('',(0.,1.,0.));
#5981=DIRECTION('center_axis',(0.,1.,0.));
#5982=DIRECTION('ref_axis',(1.,0.,0.));
#5983=DIRECTION('center_axis',(0.,-1.,0.));
#5984=DIRECTION('ref_axis',(1.,0.,0.));
#5985=DIRECTION('',(-0.707106781186547,0.707106781186548,-8.65956056235493E-17));
#5986=DIRECTION('center_axis',(0.,-1.,0.));
#5987=DIRECTION('ref_axis',(0.,0.,-1.));
#5988=DIRECTION('center_axis',(0.,-1.,0.));
#5989=DIRECTION('ref_axis',(1.,0.,0.));
#5990=DIRECTION('center_axis',(0.,1.,0.));
#5991=DIRECTION('ref_axis',(1.,0.,0.));
#5992=DIRECTION('center_axis',(0.,1.,0.));
#5993=DIRECTION('ref_axis',(1.,0.,0.));
#5994=DIRECTION('',(-0.447213595499958,0.894427190999916,-5.47678698264203E-17));
#5995=DIRECTION('center_axis',(0.,-1.,0.));
#5996=DIRECTION('ref_axis',(1.,0.,0.));
#5997=DIRECTION('',(0.,1.,0.));
#8531=CARTESIAN_POINT('',(0.,0.,0.));
#8532=CARTESIAN_POINT('Origin',(0.144337567297406,-0.6,-0.25));
#8533=CARTESIAN_POINT('',(0.288675134594813,-0.6,0.));
#8534=CARTESIAN_POINT('',(0.144337567297406,-0.6,-0.25));
#8535=CARTESIAN_POINT('',(0.288675134594813,-0.6,0.));
#8536=CARTESIAN_POINT('',(0.144337567297406,-0.96,-0.25));
#8537=CARTESIAN_POINT('',(0.144337567297406,-0.6,-0.25));
#8538=CARTESIAN_POINT('',(0.288675134594813,-0.96,0.));
#8539=CARTESIAN_POINT('',(0.288675134594813,-0.96,0.));
#8540=CARTESIAN_POINT('',(0.288675134594813,-0.6,0.));
#8541=CARTESIAN_POINT('Origin',(-0.144337567297406,-0.6,-0.25));
#8542=CARTESIAN_POINT('',(-0.144337567297406,-0.6,-0.25));
#8543=CARTESIAN_POINT('',(0.144337567297406,-0.6,-0.25));
#8544=CARTESIAN_POINT('',(-0.144337567297406,-0.96,-0.25));
#8545=CARTESIAN_POINT('',(-0.144337567297406,-0.6,-0.25));
#8546=CARTESIAN_POINT('',(0.144337567297406,-0.96,-0.25));
#8547=CARTESIAN_POINT('Origin',(-0.288675134594813,-0.6,-8.32667268468867E-17));
#8548=CARTESIAN_POINT('',(-0.288675134594813,-0.6,-3.53525079574969E-17));
#8549=CARTESIAN_POINT('',(-0.144337567297406,-0.6,-0.25));
#8550=CARTESIAN_POINT('',(-0.288675134594813,-0.96,-5.55111512312578E-17));
#8551=CARTESIAN_POINT('',(-0.288675134594813,-0.6,-3.53525079574969E-17));
#8552=CARTESIAN_POINT('',(-0.144337567297406,-0.96,-0.25));
#8553=CARTESIAN_POINT('Origin',(-0.144337567297407,-0.6,0.25));
#8554=CARTESIAN_POINT('',(-0.144337567297407,-0.6,0.25));
#8555=CARTESIAN_POINT('',(-0.288675134594813,-0.6,-3.53525079574969E-17));
#8556=CARTESIAN_POINT('',(-0.144337567297407,-0.96,0.25));
#8557=CARTESIAN_POINT('',(-0.144337567297407,-0.6,0.25));
#8558=CARTESIAN_POINT('',(-0.288675134594813,-0.96,-3.53525079574969E-17));
#8559=CARTESIAN_POINT('Origin',(0.144337567297406,-0.6,0.25));
#8560=CARTESIAN_POINT('',(0.144337567297406,-0.6,0.25));
#8561=CARTESIAN_POINT('',(-0.144337567297407,-0.6,0.25));
#8562=CARTESIAN_POINT('',(0.144337567297406,-0.96,0.25));
#8563=CARTESIAN_POINT('',(0.144337567297406,-0.6,0.25));
#8564=CARTESIAN_POINT('',(-0.144337567297407,-0.96,0.25));
#8565=CARTESIAN_POINT('Origin',(0.288675134594813,-0.6,0.));
#8566=CARTESIAN_POINT('',(0.144337567297406,-0.6,0.25));
#8567=CARTESIAN_POINT('',(0.144337567297406,-0.96,0.25));
#8568=CARTESIAN_POINT('Origin',(0.,-0.6,0.));
#8569=CARTESIAN_POINT('Origin',(0.,-0.96,0.));
#8570=CARTESIAN_POINT('Origin',(0.,-1.8,0.));
#8571=CARTESIAN_POINT('',(-0.2942,-1.8,3.60291088309151E-17));
#8572=CARTESIAN_POINT('Origin',(0.,-1.8,0.));
#8573=CARTESIAN_POINT('Origin',(0.45,0.6,0.));
#8574=CARTESIAN_POINT('',(-0.45,0.6,-5.51091059616309E-17));
#8575=CARTESIAN_POINT('Origin',(0.,0.6,0.));
#8576=CARTESIAN_POINT('Origin',(0.,0.575,0.));
#8577=CARTESIAN_POINT('',(-0.5,0.55,-6.12323399573677E-17));
#8578=CARTESIAN_POINT('Origin',(0.,0.55,0.));
#8579=CARTESIAN_POINT('',(-0.475,0.575,-5.81707229594993E-17));
#8580=CARTESIAN_POINT('Origin',(0.,0.29,0.));
#8581=CARTESIAN_POINT('',(-0.5,0.0299999999999998,-6.12323399573677E-17));
#8582=CARTESIAN_POINT('Origin',(0.,0.0299999999999998,0.));
#8583=CARTESIAN_POINT('',(-0.5,0.29,-6.12323399573677E-17));
#8584=CARTESIAN_POINT('Origin',(0.,0.0150000000000001,0.));
#8585=CARTESIAN_POINT('',(-0.47,7.11236625150491E-17,-5.75583995599256E-17));
#8586=CARTESIAN_POINT('Origin',(0.,0.,0.));
#8587=CARTESIAN_POINT('',(-0.485,0.0150000000000001,-5.93953697586466E-17));
#8588=CARTESIAN_POINT('Origin',(0.32,0.,0.));
#8589=CARTESIAN_POINT('',(-0.32,-6.93889390390723E-18,-3.91886975727153E-17));
#8590=CARTESIAN_POINT('Origin',(0.,0.,0.));
#8591=CARTESIAN_POINT('Origin',(0.,-0.02,0.));
#8592=CARTESIAN_POINT('',(-0.2942,-0.0515999999999999,3.60291088309151E-17));
#8593=CARTESIAN_POINT('Origin',(0.,-0.0515999999999999,0.));
#8594=CARTESIAN_POINT('',(-0.31,-0.02,-3.7964050773568E-17));
#8595=CARTESIAN_POINT('Origin',(0.,-1.24,0.));
#8596=CARTESIAN_POINT('',(-0.2942,-1.24,-3.60291088309151E-17));
#9969=UNCERTAINTY_MEASURE_WITH_UNIT(LENGTH_MEASURE(0.001),#10021,
'DISTANCE_ACCURACY_VALUE',
'Maximum model space distance between geometric entities at asserted c
onnectivities');
#9987=UNCERTAINTY_MEASURE_WITH_UNIT(LENGTH_MEASURE(0.001),#10021,
'DISTANCE_ACCURACY_VALUE',
'Maximum model space distance between geometric entities at asserted c
onnectivities');
#10002=(
GEOMETRIC_REPRESENTATION_CONTEXT(3)
GLOBAL_UNCERTAINTY_ASSIGNED_CONTEXT((#9969))
GLOBAL_UNIT_ASSIGNED_CONTEXT((#10021,#10023,#10024))
REPRESENTATION_CONTEXT('','3D')
);
#10020=(
GEOMETRIC_REPRESENTATION_CONTEXT(3)
GLOBAL_UNCERTAINTY_ASSIGNED_CONTEXT((#9987))
GLOBAL_UNIT_ASSIGNED_CONTEXT((#10021,#10023,#10024))
REPRESENTATION_CONTEXT('','3D')
);
#10021=(
LENGTH_UNIT()
NAMED_UNIT(*)
SI_UNIT(.CENTI.,.METRE.)
);
#10023=(
NAMED_UNIT(*)
PLANE_ANGLE_UNIT()
SI_UNIT($,.RADIAN.)
);
#10024=(
NAMED_UNIT(*)
SI_UNIT($,.STERADIAN.)
SOLID_ANGLE_UNIT()
);
#10039=SHAPE_DEFINITION_REPRESENTATION(#10071,#10149);
#10071=PRODUCT_DEFINITION_SHAPE('',$,#10182);
#10149=SHAPE_REPRESENTATION('',(#5060),#10002);
#10167=PRODUCT_DEFINITION_CONTEXT('part definition',#10265,'design');
#10182=PRODUCT_DEFINITION('M6x18 mounting screw','M6x18 mounting screw',
#10214,#10167);
#10214=PRODUCT_DEFINITION_FORMATION('',$,#10281);
#10265=APPLICATION_CONTEXT(
'Core Data for Automotive Mechanical Design Process');
#10266=PRODUCT_CONTEXT('part definition',#10265,'mechanical');
#10281=PRODUCT('M6x18 mounting screw','M6x18 mounting screw',
'M6x18 mounting screw',(#10266));
#10369=COLOUR_RGB('Black',0.12,0.14,0.17);
#10370=FILL_AREA_STYLE_COLOUR('',#10369);
#10371=FILL_AREA_STYLE('',(#10370));
#10372=SURFACE_STYLE_FILL_AREA(#10371);
#10373=SURFACE_SIDE_STYLE('',(#10372));
#10374=SURFACE_STYLE_USAGE(.BOTH.,#10373);
#10375=PRESENTATION_STYLE_ASSIGNMENT((#10374));
ENDSEC;
END-ISO-10303-21;
